ISO-10303-21;
HEADER;
FILE_DESCRIPTION (('STEP AP214'),
    '1' );
FILE_NAME ('Stator.step',
    '2026-10-24T11:32:06',
    ( '' ),
    ( '' ),
    'SwSTEP 2.0',
    'SolidWorks 2025',
    '' );
FILE_SCHEMA (( 'AUTOMOTIVE_DESIGN' ));
ENDSEC;

DATA;
#53=DIMENSIONAL_EXPONENTS ( 1.000000000000000000, 0.000000000000000000, 0.000000000000000000, 0.000000000000000000, 0.000000000000000000, 0.000000000000000000, 0.000000000000000000 ) ;
#143=ORIENTED_EDGE ( 'NONE', *, *, #7966, .T. ) ;
#167=DIRECTION ( 'NONE',  ( -0.000000000000000000, -1.000000000000000000, -0.000000000000000000 ) ) ;
#485=ADVANCED_FACE ( 'NONE', ( #1346 ), #4459, .F. ) ;
#736=CARTESIAN_POINT ( 'NONE',  ( 0.000000000000000000, 2.755905511811023612, 0.000000000000000000 ) ) ;
#1346=FACE_OUTER_BOUND ( 'NONE', #32458, .T. ) ;
#1495=CIRCLE ( 'NONE', #19606, 0.8858267716535433989 ) ;
#1909=FACE_BOUND ( 'NONE', #41553, .T. ) ;
#1942=PRODUCT_DEFINITION_CONTEXT ( 'detailed design', #14403, 'design' ) ;
#2065=EDGE_LOOP ( 'NONE', ( #23297, #143 ) ) ;
#2445=VERTEX_POINT ( 'NONE', #7303 ) ;
#2460=UNCERTAINTY_MEASURE_WITH_UNIT (LENGTH_MEASURE( 1.000000000000000082E-05 ), #9874, 'distance_accuracy_value', 'NONE');
#2666=DIRECTION ( 'NONE',  ( 0.000000000000000000, 0.000000000000000000, -1.000000000000000000 ) ) ;
#2865=APPLICATION_CONTEXT ( 'automotive_design' ) ;
#3111=DIRECTION ( 'NONE',  ( 0.000000000000000000, 1.000000000000000000, 0.000000000000000000 ) ) ;
#3119=DIRECTION ( 'NONE',  ( 0.000000000000000000, 0.000000000000000000, 1.000000000000000000 ) ) ;
#3278=AXIS2_PLACEMENT_3D ( 'NONE', #49300, #3111, #49797 ) ;
#3522=FACE_OUTER_BOUND ( 'NONE', #30560, .T. ) ;
#3793=EDGE_LOOP ( 'NONE', ( #29626, #45828, #5865, #26585 ) ) ;
#4102=DIRECTION ( 'NONE',  ( -0.000000000000000000, -1.000000000000000000, -0.000000000000000000 ) ) ;
#4313=CARTESIAN_POINT ( 'NONE',  ( 2.531258147843939089E-16, 2.755905511811023612, 2.066929133858268042 ) ) ;
#4350=CYLINDRICAL_SURFACE ( 'NONE', #16507, 2.066929133858268042 ) ;
#4459=CYLINDRICAL_SURFACE ( 'NONE', #48520, 0.8858267716535433989 ) ;
#4563=CARTESIAN_POINT ( 'NONE',  ( 1.084824920504545324E-16, 2.755905511811023612, 0.8858267716535433989 ) ) ;
#4685=( LENGTH_UNIT ( ) NAMED_UNIT ( * ) SI_UNIT ( $, .METRE. ) );
#5261=EDGE_CURVE ( 'NONE', #25678, #17533, #34414, .T. ) ;
#5865=ORIENTED_EDGE ( 'NONE', *, *, #28004, .F. ) ;
#5884=AXIS2_PLACEMENT_3D ( 'NONE', #34531, #27271, #10523 ) ;
#6574=AXIS2_PLACEMENT_3D ( 'NONE', #6792, #45752, #2666 ) ;
#6792=CARTESIAN_POINT ( 'NONE',  ( 0.000000000000000000, 2.755905511811023612, 0.000000000000000000 ) ) ;
#7151=FACE_BOUND ( 'NONE', #40983, .T. ) ;
#7303=CARTESIAN_POINT ( 'NONE',  ( 1.084824920504545324E-16, 0.000000000000000000, 0.8858267716535433989 ) ) ;
#7813=ORIENTED_EDGE ( 'NONE', *, *, #13103, .T. ) ;
#7966=EDGE_CURVE ( 'NONE', #17533, #25678, #37220, .T. ) ;
#8098=CLOSED_SHELL ( 'NONE', ( #30526, #35131, #44291, #14092, #37450, #485 ) ) ;
#8531=ORIENTED_EDGE ( 'NONE', *, *, #12688, .T. ) ;
#8554=( NAMED_UNIT ( * ) SI_UNIT ( $, .STERADIAN. ) SOLID_ANGLE_UNIT ( ) );
#8809=( CONVERSION_BASED_UNIT ( 'INCH', #39790 ) LENGTH_UNIT ( ) NAMED_UNIT ( #53 ) );
#9660=PLANE ( 'NONE',  #51014 ) ;
#9874=( CONVERSION_BASED_UNIT ( 'INCH', #14248 ) LENGTH_UNIT ( ) NAMED_UNIT ( #15895 ) );
#10321=VERTEX_POINT ( 'NONE', #31427 ) ;
#10523=DIRECTION ( 'NONE',  ( 0.000000000000000000, 0.000000000000000000, 1.000000000000000000 ) ) ;
#11200=( GEOMETRIC_REPRESENTATION_CONTEXT ( 3 ) GLOBAL_UNCERTAINTY_ASSIGNED_CONTEXT ( ( #28278 ) ) GLOBAL_UNIT_ASSIGNED_CONTEXT ( ( #8809, #43397, #8554 ) ) REPRESENTATION_CONTEXT ( 'NONE', 'WORKASPACE' ) );
#11319=ORIENTED_EDGE ( 'NONE', *, *, #38927, .F. ) ;
#11350=ORIENTED_EDGE ( 'NONE', *, *, #13103, .F. ) ;
#12205=DIRECTION ( 'NONE',  ( 0.000000000000000000, 0.000000000000000000, -1.000000000000000000 ) ) ;
#12476=CARTESIAN_POINT ( 'NONE',  ( 0.000000000000000000, 2.755905511811023612, 0.000000000000000000 ) ) ;
#12688=EDGE_CURVE ( 'NONE', #13074, #18617, #32709, .T. ) ;
#13026=DIRECTION ( 'NONE',  ( 0.000000000000000000, 1.000000000000000000, 0.000000000000000000 ) ) ;
#13074=VERTEX_POINT ( 'NONE', #4563 ) ;
#13103=EDGE_CURVE ( 'NONE', #25678, #32755, #39674, .T. ) ;
#13229=CARTESIAN_POINT ( 'NONE',  ( 0.000000000000000000, 2.755905511811023612, 0.000000000000000000 ) ) ;
#13567=( GEOMETRIC_REPRESENTATION_CONTEXT ( 3 ) GLOBAL_UNCERTAINTY_ASSIGNED_CONTEXT ( ( #2460 ) ) GLOBAL_UNIT_ASSIGNED_CONTEXT ( ( #9874, #41876, #17617 ) ) REPRESENTATION_CONTEXT ( 'NONE', 'WORKASPACE' ) );
#14092=ADVANCED_FACE ( 'NONE', ( #3522, #7151 ), #35027, .F. ) ;
#14248=LENGTH_MEASURE_WITH_UNIT ( LENGTH_MEASURE( 0.02539999999999999897 ), #49570 );
#14403=APPLICATION_CONTEXT ( 'automotive_design' ) ;
#14509=SHAPE_REPRESENTATION_RELATIONSHIP ( 'NONE' , 'NONE' ,  #36385, #31660 ) ;
#14516=STYLED_ITEM('',(#51101),#24040);
#14612=PRODUCT_DEFINITION ( 'UNKNOWN', '', #15210, #1942 ) ;
#14797=VERTEX_POINT ( 'NONE', #41379 ) ;
#15210=PRODUCT_DEFINITION_FORMATION_WITH_SPECIFIED_SOURCE ( 'ANY', '', #43784, .NOT_KNOWN. ) ;
#15421=DIRECTION ( 'NONE',  ( 0.000000000000000000, 0.000000000000000000, -1.000000000000000000 ) ) ;
#15895=DIMENSIONAL_EXPONENTS ( 1.000000000000000000, 0.000000000000000000, 0.000000000000000000, 0.000000000000000000, 0.000000000000000000, 0.000000000000000000, 0.000000000000000000 ) ;
#16236=CARTESIAN_POINT ( 'NONE',  ( 1.084824920504545324E-16, 2.755905511811023612, 0.8858267716535433989 ) ) ;
#16486=DIRECTION ( 'NONE',  ( 0.000000000000000000, 0.000000000000000000, -1.000000000000000000 ) ) ;
#16507=AXIS2_PLACEMENT_3D ( 'NONE', #736, #4102, #16486 ) ;
#16614=PRODUCT_DEFINITION_SHAPE ( 'NONE', 'NONE',  #14612 ) ;
#16875=DIRECTION ( 'NONE',  ( 0.000000000000000000, 0.000000000000000000, 1.000000000000000000 ) ) ;
#16879=AXIS2_PLACEMENT_3D ( 'NONE', #12476, #23588, #16875 ) ;
#17154=CARTESIAN_POINT ( 'NONE',  ( 0.000000000000000000, 2.755905511811023612, 0.000000000000000000 ) ) ;
#17432=CIRCLE ( 'NONE', #5884, 0.8858267716535433989 ) ;
#17533=VERTEX_POINT ( 'NONE', #4313 ) ;
#17617=( NAMED_UNIT ( * ) SI_UNIT ( $, .STERADIAN. ) SOLID_ANGLE_UNIT ( ) );
#17949=ORIENTED_EDGE ( 'NONE', *, *, #38927, .T. ) ;
#17967=EDGE_LOOP ( 'NONE', ( #34372, #46874, #33197, #11350 ) ) ;
#18397=DIRECTION ( 'NONE',  ( 1.000000000000000000, 0.000000000000000000, 0.000000000000000000 ) ) ;
#18511=AXIS2_PLACEMENT_3D ( 'NONE', #42775, #46872, #15421 ) ;
#18617=VERTEX_POINT ( 'NONE', #38431 ) ;
#19326=CIRCLE ( 'NONE', #16879, 0.8858267716535433989 ) ;
#19606=AXIS2_PLACEMENT_3D ( 'NONE', #29906, #30924, #27029 ) ;
#19817=DIRECTION ( 'NONE',  ( 1.000000000000000000, 0.000000000000000000, 0.000000000000000000 ) ) ;
#20215=VECTOR ( 'NONE', #31994, 39.37007874015748143 ) ;
#20467=DIRECTION ( 'NONE',  ( 0.000000000000000000, 0.000000000000000000, 1.000000000000000000 ) ) ;
#20597=DIRECTION ( 'NONE',  ( 0.000000000000000000, 1.000000000000000000, 0.000000000000000000 ) ) ;
#20984=CARTESIAN_POINT ( 'NONE',  ( 0.000000000000000000, 0.000000000000000000, 0.000000000000000000 ) ) ;
#21280=DIRECTION ( 'NONE',  ( 0.000000000000000000, -0.000000000000000000, 1.000000000000000000 ) ) ;
#21751=CIRCLE ( 'NONE', #39022, 2.066929133858268042 ) ;
#22472=EDGE_CURVE ( 'NONE', #18617, #13074, #19326, .T. ) ;
#22537=CYLINDRICAL_SURFACE ( 'NONE', #6574, 2.066929133858268042 ) ;
#22793=FACE_OUTER_BOUND ( 'NONE', #17967, .T. ) ;
#23269=LINE ( 'NONE', #50831, #47228 ) ;
#23297=ORIENTED_EDGE ( 'NONE', *, *, #5261, .T. ) ;
#23463=ORIENTED_EDGE ( 'NONE', *, *, #28004, .T. ) ;
#23588=DIRECTION ( 'NONE',  ( 0.000000000000000000, 1.000000000000000000, 0.000000000000000000 ) ) ;
#23677=EDGE_CURVE ( 'NONE', #18617, #14797, #50461, .T. ) ;
#24040=MANIFOLD_SOLID_BREP ( 'Extrude-Thin1', #8098 ) ;
#24077=DIRECTION ( 'NONE',  ( -0.000000000000000000, -1.000000000000000000, -0.000000000000000000 ) ) ;
#24363=CARTESIAN_POINT ( 'NONE',  ( 0.000000000000000000, 2.755905511811023612, -2.066929133858268042 ) ) ;
#24704=CARTESIAN_POINT ( 'NONE',  ( 0.000000000000000000, 2.755905511811023612, -2.066929133858268042 ) ) ;
#24760=DIRECTION ( 'NONE',  ( 1.000000000000000000, 0.000000000000000000, 0.000000000000000000 ) ) ;
#25647=ORIENTED_EDGE ( 'NONE', *, *, #29630, .F. ) ;
#25678=VERTEX_POINT ( 'NONE', #24363 ) ;
#26134=ORIENTED_EDGE ( 'NONE', *, *, #23677, .T. ) ;
#26155=AXIS2_PLACEMENT_3D ( 'NONE', #36638, #33281, #24760 ) ;
#26257=CARTESIAN_POINT ( 'NONE',  ( 0.000000000000000000, 0.000000000000000000, 0.000000000000000000 ) ) ;
#26585=ORIENTED_EDGE ( 'NONE', *, *, #23677, .F. ) ;
#26741=AXIS2_PLACEMENT_3D ( 'NONE', #20984, #20467, #36229 ) ;
#27029=DIRECTION ( 'NONE',  ( 0.000000000000000000, 0.000000000000000000, 1.000000000000000000 ) ) ;
#27271=DIRECTION ( 'NONE',  ( 0.000000000000000000, 1.000000000000000000, 0.000000000000000000 ) ) ;
#27320=FACE_OUTER_BOUND ( 'NONE', #38482, .T. ) ;
#27501=ORIENTED_EDGE ( 'NONE', *, *, #32940, .F. ) ;
#27627=SHAPE_DEFINITION_REPRESENTATION ( #16614, #36385 ) ;
#28004=EDGE_CURVE ( 'NONE', #14797, #2445, #1495, .T. ) ;
#28038=CARTESIAN_POINT ( 'NONE',  ( 0.000000000000000000, 2.755905511811023612, -0.8858267716535433989 ) ) ;
#28154=DIRECTION ( 'NONE',  ( -0.000000000000000000, -1.000000000000000000, -0.000000000000000000 ) ) ;
#28278=UNCERTAINTY_MEASURE_WITH_UNIT (LENGTH_MEASURE( 1.000000000000000082E-05 ), #8809, 'distance_accuracy_value', 'NONE');
#29626=ORIENTED_EDGE ( 'NONE', *, *, #22472, .T. ) ;
#29630=EDGE_CURVE ( 'NONE', #10321, #32755, #21751, .T. ) ;
#29670=EDGE_CURVE ( 'NONE', #17533, #10321, #23269, .T. ) ;
#29906=CARTESIAN_POINT ( 'NONE',  ( 0.000000000000000000, 0.000000000000000000, 0.000000000000000000 ) ) ;
#30526=ADVANCED_FACE ( 'NONE', ( #39160 ), #43531, .F. ) ;
#30560=EDGE_LOOP ( 'NONE', ( #36705, #25647 ) ) ;
#30898=DIRECTION ( 'NONE',  ( 0.000000000000000000, -0.000000000000000000, 1.000000000000000000 ) ) ;
#30924=DIRECTION ( 'NONE',  ( 0.000000000000000000, 1.000000000000000000, 0.000000000000000000 ) ) ;
#30995=ORIENTED_EDGE ( 'NONE', *, *, #22472, .F. ) ;
#31427=CARTESIAN_POINT ( 'NONE',  ( 2.531258147843939089E-16, 0.000000000000000000, 2.066929133858268042 ) ) ;
#31660=ADVANCED_BREP_SHAPE_REPRESENTATION ( '', ( #24040, #26741 ), #13567 ) ;
#31994=DIRECTION ( 'NONE',  ( -0.000000000000000000, -1.000000000000000000, -0.000000000000000000 ) ) ;
#32458=EDGE_LOOP ( 'NONE', ( #27501, #8531, #26134, #11319 ) ) ;
#32625=VECTOR ( 'NONE', #167, 39.37007874015748143 ) ;
#32709=CIRCLE ( 'NONE', #40013, 0.8858267716535433989 ) ;
#32755=VERTEX_POINT ( 'NONE', #34595 ) ;
#32940=EDGE_CURVE ( 'NONE', #13074, #2445, #47688, .T. ) ;
#33197=ORIENTED_EDGE ( 'NONE', *, *, #29630, .T. ) ;
#33281=DIRECTION ( 'NONE',  ( 0.000000000000000000, 1.000000000000000000, 0.000000000000000000 ) ) ;
#33899=CARTESIAN_POINT ( 'NONE',  ( 0.000000000000000000, 0.000000000000000000, 0.000000000000000000 ) ) ;
#34372=ORIENTED_EDGE ( 'NONE', *, *, #7966, .F. ) ;
#34414=CIRCLE ( 'NONE', #26155, 2.066929133858268042 ) ;
#34531=CARTESIAN_POINT ( 'NONE',  ( 0.000000000000000000, 0.000000000000000000, 0.000000000000000000 ) ) ;
#34595=CARTESIAN_POINT ( 'NONE',  ( 0.000000000000000000, 0.000000000000000000, -2.066929133858268042 ) ) ;
#35027=PLANE ( 'NONE',  #38444 ) ;
#35131=ADVANCED_FACE ( 'NONE', ( #22793 ), #22537, .T. ) ;
#35881=VECTOR ( 'NONE', #47627, 39.37007874015748143 ) ;
#36216=CARTESIAN_POINT ( 'NONE',  ( 0.000000000000000000, 2.755905511811023612, 0.000000000000000000 ) ) ;
#36229=DIRECTION ( 'NONE',  ( 1.000000000000000000, 0.000000000000000000, 0.000000000000000000 ) ) ;
#36385=SHAPE_REPRESENTATION ( 'Stator', ( #26741 ), #13567 ) ;
#36638=CARTESIAN_POINT ( 'NONE',  ( 0.000000000000000000, 2.755905511811023612, 0.000000000000000000 ) ) ;
#36705=ORIENTED_EDGE ( 'NONE', *, *, #44830, .F. ) ;
#36774=FACE_OUTER_BOUND ( 'NONE', #2065, .T. ) ;
#37220=CIRCLE ( 'NONE', #46243, 2.066929133858268042 ) ;
#37450=ADVANCED_FACE ( 'NONE', ( #27320 ), #4350, .T. ) ;
#38417=ORIENTED_EDGE ( 'NONE', *, *, #5261, .F. ) ;
#38431=CARTESIAN_POINT ( 'NONE',  ( 0.000000000000000000, 2.755905511811023612, -0.8858267716535433989 ) ) ;
#38441=MECHANICAL_DESIGN_GEOMETRIC_PRESENTATION_REPRESENTATION('',(#14516),#11200);
#38444=AXIS2_PLACEMENT_3D ( 'NONE', #26257, #46601, #30898 ) ;
#38482=EDGE_LOOP ( 'NONE', ( #47991, #38417, #7813, #49113 ) ) ;
#38927=EDGE_CURVE ( 'NONE', #2445, #14797, #17432, .T. ) ;
#39022=AXIS2_PLACEMENT_3D ( 'NONE', #33899, #41892, #18397 ) ;
#39160=FACE_OUTER_BOUND ( 'NONE', #3793, .T. ) ;
#39513=PRODUCT_CONTEXT ( 'NONE', #2865, 'mechanical' ) ;
#39674=LINE ( 'NONE', #24704, #32625 ) ;
#39790=LENGTH_MEASURE_WITH_UNIT ( LENGTH_MEASURE( 0.02539999999999999897 ), #4685 );
#40013=AXIS2_PLACEMENT_3D ( 'NONE', #13229, #44693, #3119 ) ;
#40983=EDGE_LOOP ( 'NONE', ( #23463, #17949 ) ) ;
#41220=CIRCLE ( 'NONE', #3278, 2.066929133858268042 ) ;
#41379=CARTESIAN_POINT ( 'NONE',  ( 0.000000000000000000, 0.000000000000000000, -0.8858267716535433989 ) ) ;
#41553=EDGE_LOOP ( 'NONE', ( #30995, #50255 ) ) ;
#41876=( NAMED_UNIT ( * ) PLANE_ANGLE_UNIT ( ) SI_UNIT ( $, .RADIAN. ) );
#41892=DIRECTION ( 'NONE',  ( 0.000000000000000000, 1.000000000000000000, 0.000000000000000000 ) ) ;
#42775=CARTESIAN_POINT ( 'NONE',  ( 0.000000000000000000, 2.755905511811023612, 0.000000000000000000 ) ) ;
#43397=( NAMED_UNIT ( * ) PLANE_ANGLE_UNIT ( ) SI_UNIT ( $, .RADIAN. ) );
#43531=CYLINDRICAL_SURFACE ( 'NONE', #18511, 0.8858267716535433989 ) ;
#43567=CARTESIAN_POINT ( 'NONE',  ( 0.000000000000000000, 2.755905511811023612, 0.000000000000000000 ) ) ;
#43784=PRODUCT ( 'Stator', 'Stator', '', ( #39513 ) ) ;
#44291=ADVANCED_FACE ( 'NONE', ( #36774, #1909 ), #9660, .T. ) ;
#44693=DIRECTION ( 'NONE',  ( 0.000000000000000000, 1.000000000000000000, 0.000000000000000000 ) ) ;
#44830=EDGE_CURVE ( 'NONE', #32755, #10321, #41220, .T. ) ;
#45752=DIRECTION ( 'NONE',  ( -0.000000000000000000, -1.000000000000000000, -0.000000000000000000 ) ) ;
#45828=ORIENTED_EDGE ( 'NONE', *, *, #32940, .T. ) ;
#46243=AXIS2_PLACEMENT_3D ( 'NONE', #43567, #20597, #19817 ) ;
#46601=DIRECTION ( 'NONE',  ( 0.000000000000000000, 1.000000000000000000, 0.000000000000000000 ) ) ;
#46872=DIRECTION ( 'NONE',  ( -0.000000000000000000, -1.000000000000000000, -0.000000000000000000 ) ) ;
#46874=ORIENTED_EDGE ( 'NONE', *, *, #29670, .T. ) ;
#47228=VECTOR ( 'NONE', #28154, 39.37007874015748143 ) ;
#47627=DIRECTION ( 'NONE',  ( -0.000000000000000000, -1.000000000000000000, -0.000000000000000000 ) ) ;
#47688=LINE ( 'NONE', #16236, #20215 ) ;
#47991=ORIENTED_EDGE ( 'NONE', *, *, #29670, .F. ) ;
#48520=AXIS2_PLACEMENT_3D ( 'NONE', #36216, #24077, #12205 ) ;
#49113=ORIENTED_EDGE ( 'NONE', *, *, #44830, .T. ) ;
#49300=CARTESIAN_POINT ( 'NONE',  ( 0.000000000000000000, 0.000000000000000000, 0.000000000000000000 ) ) ;
#49570=( LENGTH_UNIT ( ) NAMED_UNIT ( * ) SI_UNIT ( $, .METRE. ) );
#49797=DIRECTION ( 'NONE',  ( 1.000000000000000000, 0.000000000000000000, 0.000000000000000000 ) ) ;
#50255=ORIENTED_EDGE ( 'NONE', *, *, #12688, .F. ) ;
#50461=LINE ( 'NONE', #28038, #35881 ) ;
#50831=CARTESIAN_POINT ( 'NONE',  ( 2.531258147843939089E-16, 2.755905511811023612, 2.066929133858268042 ) ) ;
#51014=AXIS2_PLACEMENT_3D ( 'NONE', #17154, #13026, #21280 ) ;
#51095=COLOUR_RGB('Off White',0.89,0.88,0.83);
#51096=FILL_AREA_STYLE_COLOUR('',#51095);
#51097=FILL_AREA_STYLE('',(#51096));
#51098=SURFACE_STYLE_FILL_AREA(#51097);
#51099=SURFACE_SIDE_STYLE('',(#51098));
#51100=SURFACE_STYLE_USAGE(.BOTH.,#51099);
#51101=PRESENTATION_STYLE_ASSIGNMENT((#51100));
ENDSEC;
END-ISO-10303-21;
